ISO-10303-21;
HEADER;
/* Generated by software containing ST-Developer
 * from STEP Tools, Inc. (www.steptools.com) 
 */

FILE_DESCRIPTION(
/* description */ ('Independent compact industrial fixture table, bolted aluminum worktop
 on connected adjustable support base. Whole-mm nominal dimensions. No
 load rating assigned.'),
/* implementation_level */ '2;1');

FILE_NAME(
/* name */ 'Flat washer M8.step',
/* time_stamp */ '2026-11-07T17:47:58-08:00',
/* author */ (''),
/* organization */ (''),
/* preprocessor_version */ 'ST-DEVELOPER v20.2',
/* originating_system */ 'Autodesk Translation Framework v15.17.0.0',
/* authorisation */ '');

FILE_SCHEMA (('AUTOMOTIVE_DESIGN { 1 0 10303 214 3 1 1 }'));
ENDSEC;

DATA;
#10=MECHANICAL_DESIGN_GEOMETRIC_PRESENTATION_REPRESENTATION('',(#2254),#97475);
#2216=SHAPE_REPRESENTATION_RELATIONSHIP('SRR','None',#97609,#2235);
#2235=ADVANCED_BREP_SHAPE_REPRESENTATION('',(#2273),#97459);
#2254=STYLED_ITEM('',(#97721),#2273);
#2273=MANIFOLD_SOLID_BREP('Body1',#21815);
#2314=FACE_BOUND('',#3896,.T.);
#2315=FACE_BOUND('',#3898,.T.);
#2415=PLANE('',#22254);
#2416=PLANE('',#22255);
#2713=FACE_OUTER_BOUND('',#3893,.T.);
#2714=FACE_OUTER_BOUND('',#3894,.T.);
#2715=FACE_OUTER_BOUND('',#3895,.T.);
#2716=FACE_OUTER_BOUND('',#3897,.T.);
#3893=EDGE_LOOP('',(#14108,#14109,#14110,#14111));
#3894=EDGE_LOOP('',(#14112,#14113,#14114,#14115));
#3895=EDGE_LOOP('',(#14116));
#3896=EDGE_LOOP('',(#14117));
#3897=EDGE_LOOP('',(#14118));
#3898=EDGE_LOOP('',(#14119));
#5134=LINE('',#37288,#6348);
#5135=LINE('',#37294,#6349);
#6348=VECTOR('',#24120,4.5);
#6349=VECTOR('',#24127,9.);
#7399=CIRCLE('',#22249,4.5);
#7400=CIRCLE('',#22250,4.5);
#7401=CIRCLE('',#22252,9.);
#7402=CIRCLE('',#22253,9.);
#7945=VERTEX_POINT('',#37285);
#7946=VERTEX_POINT('',#37287);
#7947=VERTEX_POINT('',#37291);
#7948=VERTEX_POINT('',#37293);
#10311=EDGE_CURVE('',#7945,#7945,#7399,.T.);
#10312=EDGE_CURVE('',#7945,#7946,#5134,.T.);
#10313=EDGE_CURVE('',#7946,#7946,#7400,.T.);
#10314=EDGE_CURVE('',#7947,#7947,#7401,.T.);
#10315=EDGE_CURVE('',#7947,#7948,#5135,.T.);
#10316=EDGE_CURVE('',#7948,#7948,#7402,.T.);
#14108=ORIENTED_EDGE('',*,*,#10311,.F.);
#14109=ORIENTED_EDGE('',*,*,#10312,.T.);
#14110=ORIENTED_EDGE('',*,*,#10313,.T.);
#14111=ORIENTED_EDGE('',*,*,#10312,.F.);
#14112=ORIENTED_EDGE('',*,*,#10314,.F.);
#14113=ORIENTED_EDGE('',*,*,#10315,.T.);
#14114=ORIENTED_EDGE('',*,*,#10316,.T.);
#14115=ORIENTED_EDGE('',*,*,#10315,.F.);
#14116=ORIENTED_EDGE('',*,*,#10314,.T.);
#14117=ORIENTED_EDGE('',*,*,#10311,.T.);
#14118=ORIENTED_EDGE('',*,*,#10316,.F.);
#14119=ORIENTED_EDGE('',*,*,#10313,.F.);
#19839=CYLINDRICAL_SURFACE('',#22248,4.5);
#19840=CYLINDRICAL_SURFACE('',#22251,9.);
#20833=ADVANCED_FACE('',(#2713),#19839,.F.);
#20834=ADVANCED_FACE('',(#2714),#19840,.T.);
#20835=ADVANCED_FACE('',(#2715,#2314),#2415,.T.);
#20836=ADVANCED_FACE('',(#2716,#2315),#2416,.F.);
#21815=CLOSED_SHELL('',(#20833,#20834,#20835,#20836));
#22247=AXIS2_PLACEMENT_3D('',#37283,#24114,#24115);
#22248=AXIS2_PLACEMENT_3D('',#37284,#24116,#24117);
#22249=AXIS2_PLACEMENT_3D('',#37286,#24118,#24119);
#22250=AXIS2_PLACEMENT_3D('',#37289,#24121,#24122);
#22251=AXIS2_PLACEMENT_3D('',#37290,#24123,#24124);
#22252=AXIS2_PLACEMENT_3D('',#37292,#24125,#24126);
#22253=AXIS2_PLACEMENT_3D('',#37295,#24128,#24129);
#22254=AXIS2_PLACEMENT_3D('',#37296,#24130,#24131);
#22255=AXIS2_PLACEMENT_3D('',#37297,#24132,#24133);
#24114=DIRECTION('axis',(0.,0.,1.));
#24115=DIRECTION('refdir',(1.,0.,0.));
#24116=DIRECTION('center_axis',(0.,0.,1.));
#24117=DIRECTION('ref_axis',(1.,0.,0.));
#24118=DIRECTION('center_axis',(0.,0.,-1.));
#24119=DIRECTION('ref_axis',(1.,0.,0.));
#24120=DIRECTION('',(0.,0.,-1.));
#24121=DIRECTION('center_axis',(0.,0.,-1.));
#24122=DIRECTION('ref_axis',(1.,0.,0.));
#24123=DIRECTION('center_axis',(0.,0.,1.));
#24124=DIRECTION('ref_axis',(1.,0.,0.));
#24125=DIRECTION('center_axis',(0.,0.,1.));
#24126=DIRECTION('ref_axis',(1.,0.,0.));
#24127=DIRECTION('',(0.,0.,-1.));
#24128=DIRECTION('center_axis',(0.,0.,1.));
#24129=DIRECTION('ref_axis',(1.,0.,0.));
#24130=DIRECTION('center_axis',(0.,0.,1.));
#24131=DIRECTION('ref_axis',(1.,0.,0.));
#24132=DIRECTION('center_axis',(0.,0.,1.));
#24133=DIRECTION('ref_axis',(1.,0.,0.));
#37283=CARTESIAN_POINT('',(0.,0.,0.));
#37284=CARTESIAN_POINT('Origin',(0.,0.,0.));
#37285=CARTESIAN_POINT('',(-4.5,-5.51091059616309E-16,2.));
#37286=CARTESIAN_POINT('Origin',(0.,0.,2.));
#37287=CARTESIAN_POINT('',(-4.5,-5.51091059616309E-16,0.));
#37288=CARTESIAN_POINT('',(-4.5,-5.51091059616309E-16,0.));
#37289=CARTESIAN_POINT('Origin',(0.,0.,0.));
#37290=CARTESIAN_POINT('Origin',(0.,0.,0.));
#37291=CARTESIAN_POINT('',(-9.,-1.10218211923262E-15,2.));
#37292=CARTESIAN_POINT('Origin',(0.,0.,2.));
#37293=CARTESIAN_POINT('',(-9.,-1.10218211923262E-15,0.));
#37294=CARTESIAN_POINT('',(-9.,-1.10218211923262E-15,0.));
#37295=CARTESIAN_POINT('Origin',(0.,0.,0.));
#37296=CARTESIAN_POINT('Origin',(0.,0.,2.));
#37297=CARTESIAN_POINT('Origin',(0.,0.,0.));
#97436=UNCERTAINTY_MEASURE_WITH_UNIT(LENGTH_MEASURE(0.01),#97476,
'DISTANCE_ACCURACY_VALUE',
'Maximum model space distance between geometric entities at asserted c
onnectivities');
#97452=UNCERTAINTY_MEASURE_WITH_UNIT(LENGTH_MEASURE(0.01),#97476,
'DISTANCE_ACCURACY_VALUE',
'Maximum model space distance between geometric entities at asserted c
onnectivities');
#97459=(
GEOMETRIC_REPRESENTATION_CONTEXT(3)
GLOBAL_UNCERTAINTY_ASSIGNED_CONTEXT((#97436))
GLOBAL_UNIT_ASSIGNED_CONTEXT((#97476,#97478,#97479))
REPRESENTATION_CONTEXT('','3D')
);
#97475=(
GEOMETRIC_REPRESENTATION_CONTEXT(3)
GLOBAL_UNCERTAINTY_ASSIGNED_CONTEXT((#97452))
GLOBAL_UNIT_ASSIGNED_CONTEXT((#97476,#97478,#97479))
REPRESENTATION_CONTEXT('','3D')
);
#97476=(
LENGTH_UNIT()
NAMED_UNIT(*)
SI_UNIT(.MILLI.,.METRE.)
);
#97478=(
NAMED_UNIT(*)
PLANE_ANGLE_UNIT()
SI_UNIT($,.RADIAN.)
);
#97479=(
NAMED_UNIT(*)
SI_UNIT($,.STERADIAN.)
SOLID_ANGLE_UNIT()
);
#97486=SHAPE_DEFINITION_REPRESENTATION(#97508,#97609);
#97508=PRODUCT_DEFINITION_SHAPE('',$,#97632);
#97609=SHAPE_REPRESENTATION('',(#22247),#97459);
#97625=PRODUCT_DEFINITION_CONTEXT('part definition',#97693,'design');
#97632=PRODUCT_DEFINITION('Flat Washer M8','Flat washer M8',#97654,#97625);
#97654=PRODUCT_DEFINITION_FORMATION('',$,#97701);
#97693=APPLICATION_CONTEXT(
'Core Data for Automotive Mechanical Design Process');
#97694=PRODUCT_CONTEXT('part definition',#97693,'mechanical');
#97701=PRODUCT('Flat Washer M8','Flat washer M8','NOT SPECIFIED',(#97694));
#97721=PRESENTATION_STYLE_ASSIGNMENT((#97728));
#97728=SURFACE_STYLE_USAGE(.BOTH.,#97735);
#97735=SURFACE_SIDE_STYLE('',(#97742));
#97742=SURFACE_STYLE_FILL_AREA(#97749);
#97749=FILL_AREA_STYLE('Light gray',(#97756));
#97756=FILL_AREA_STYLE_COLOUR('Light gray',#97763);
#97763=COLOUR_RGB('Light gray',0.725490196078431,0.752941176470588,0.792156862745098);
ENDSEC;
END-ISO-10303-21;
